ISO-10303-21;
HEADER;
FILE_DESCRIPTION((''),'2;1');
FILE_NAME('HUB_SCREW_M4.step','2026-10-01T22:05:39-07:00',(''),(''),'','','');
FILE_SCHEMA (('AUTOMOTIVE_DESIGN { 1 0 10303 214 3 1 1 }'));
ENDSEC;
DATA;
#10=MECHANICAL_DESIGN_GEOMETRIC_PRESENTATION_REPRESENTATION('',(#641),#24628);
#557=SHAPE_REPRESENTATION_RELATIONSHIP('SRR','None',#24832,#599) ;
#599=ADVANCED_BREP_SHAPE_REPRESENTATION('',(#680),#24622) ;
#641=STYLED_ITEM('',(#25030),#680) ;
#680=MANIFOLD_SOLID_BREP('HUB_SCREW_M4',#13183) ;
#942=FACE_BOUND('',#4700,.T.) ;
#1757=LINE('',#24302,#2593) ;
#1758=LINE('',#24309,#2594) ;
#2593=VECTOR('',#19444,0.195) ;
#2594=VECTOR('',#19453,0.35) ;
#2944=CYLINDRICAL_SURFACE('',#15299,0.195) ;
#2945=CYLINDRICAL_SURFACE('',#15303,0.35) ;
#3672=FACE_OUTER_BOUND('',#4695,.T.) ;
#3673=FACE_OUTER_BOUND('',#4696,.T.) ;
#3674=FACE_OUTER_BOUND('',#4697,.T.) ;
#3675=FACE_OUTER_BOUND('',#4698,.T.) ;
#3676=FACE_OUTER_BOUND('',#4699,.T.) ;
#4695=EDGE_LOOP('',(#11803,#11804,#11805,#11806)) ;
#4696=EDGE_LOOP('',(#11807)) ;
#4697=EDGE_LOOP('',(#11808,#11809,#11810,#11811)) ;
#4698=EDGE_LOOP('',(#11812)) ;
#4699=EDGE_LOOP('',(#11813)) ;
#4700=EDGE_LOOP('',(#11814)) ;
#5521=CIRCLE('',#15300,0.195) ;
#5522=CIRCLE('',#15301,0.195) ;
#5523=CIRCLE('',#15304,0.35) ;
#5524=CIRCLE('',#15305,0.35) ;
#6669=VERTEX_POINT('',#24299) ;
#6670=VERTEX_POINT('',#24301) ;
#6671=VERTEX_POINT('',#24306) ;
#6672=VERTEX_POINT('',#24308) ;
#8391=EDGE_CURVE('',#6669,#6669,#5521,.T.) ;
#8392=EDGE_CURVE('',#6669,#6670,#1757,.T.) ;
#8393=EDGE_CURVE('',#6670,#6670,#5522,.T.) ;
#8394=EDGE_CURVE('',#6671,#6671,#5523,.T.) ;
#8395=EDGE_CURVE('',#6671,#6672,#1758,.T.) ;
#8396=EDGE_CURVE('',#6672,#6672,#5524,.T.) ;
#11803=ORIENTED_EDGE('',*,*,#8391,.F.) ;
#11804=ORIENTED_EDGE('',*,*,#8392,.T.) ;
#11805=ORIENTED_EDGE('',*,*,#8393,.F.) ;
#11806=ORIENTED_EDGE('',*,*,#8392,.F.) ;
#11807=ORIENTED_EDGE('',*,*,#8391,.T.) ;
#11808=ORIENTED_EDGE('',*,*,#8394,.F.) ;
#11809=ORIENTED_EDGE('',*,*,#8395,.T.) ;
#11810=ORIENTED_EDGE('',*,*,#8396,.F.) ;
#11811=ORIENTED_EDGE('',*,*,#8395,.F.) ;
#11812=ORIENTED_EDGE('',*,*,#8396,.T.) ;
#11813=ORIENTED_EDGE('',*,*,#8394,.T.) ;
#11814=ORIENTED_EDGE('',*,*,#8393,.T.) ;
#12308=PLANE('',#15302) ;
#12309=PLANE('',#15306) ;
#12310=PLANE('',#15307) ;
#13067=ADVANCED_FACE('',(#3672),#2944,.T.) ;
#13068=ADVANCED_FACE('',(#3673),#12308,.T.) ;
#13069=ADVANCED_FACE('',(#3674),#2945,.T.) ;
#13070=ADVANCED_FACE('',(#3675),#12309,.T.) ;
#13071=ADVANCED_FACE('',(#3676,#942),#12310,.T.) ;
#13183=CLOSED_SHELL('',(#13067,#13068,#13069,#13070,#13071)) ;
#15298=AXIS2_PLACEMENT_3D('',#24297,#19438,#19439) ;
#15299=AXIS2_PLACEMENT_3D('',#24298,#19440,#19441) ;
#15300=AXIS2_PLACEMENT_3D('',#24300,#19442,#19443) ;
#15301=AXIS2_PLACEMENT_3D('',#24303,#19445,#19446) ;
#15302=AXIS2_PLACEMENT_3D('',#24304,#19447,#19448) ;
#15303=AXIS2_PLACEMENT_3D('',#24305,#19449,#19450) ;
#15304=AXIS2_PLACEMENT_3D('',#24307,#19451,#19452) ;
#15305=AXIS2_PLACEMENT_3D('',#24310,#19454,#19455) ;
#15306=AXIS2_PLACEMENT_3D('',#24311,#19456,#19457) ;
#15307=AXIS2_PLACEMENT_3D('',#24312,#19458,#19459) ;
#19438=DIRECTION('axis',(0.,0.,1.)) ;
#19439=DIRECTION('refdir',(1.,0.,0.)) ;
#19440=DIRECTION('center_axis',(0.,-1.,0.)) ;
#19441=DIRECTION('ref_axis',(1.,0.,0.)) ;
#19442=DIRECTION('center_axis',(0.,-1.,0.)) ;
#19443=DIRECTION('ref_axis',(1.,0.,0.)) ;
#19444=DIRECTION('',(0.,1.,0.)) ;
#19445=DIRECTION('center_axis',(0.,1.,0.)) ;
#19446=DIRECTION('ref_axis',(1.,0.,0.)) ;
#19447=DIRECTION('center_axis',(0.,-1.,0.)) ;
#19448=DIRECTION('ref_axis',(1.,0.,0.)) ;
#19449=DIRECTION('center_axis',(0.,-1.,0.)) ;
#19450=DIRECTION('ref_axis',(1.,0.,0.)) ;
#19451=DIRECTION('center_axis',(0.,-1.,0.)) ;
#19452=DIRECTION('ref_axis',(1.,0.,0.)) ;
#19453=DIRECTION('',(0.,1.,0.)) ;
#19454=DIRECTION('center_axis',(0.,1.,0.)) ;
#19455=DIRECTION('ref_axis',(1.,0.,0.)) ;
#19456=DIRECTION('center_axis',(0.,1.,0.)) ;
#19457=DIRECTION('ref_axis',(-1.,0.,0.)) ;
#19458=DIRECTION('center_axis',(0.,-1.,0.)) ;
#19459=DIRECTION('ref_axis',(1.,0.,0.)) ;
#24297=CARTESIAN_POINT('',(0.,0.,0.)) ;
#24298=CARTESIAN_POINT('Origin',(0.,-0.6,0.)) ;
#24299=CARTESIAN_POINT('',(-0.195,-1.2,-2.38806125833734E-17)) ;
#24300=CARTESIAN_POINT('Origin',(0.,-1.2,0.)) ;
#24301=CARTESIAN_POINT('',(-0.195,0.,-2.38806125833734E-17)) ;
#24302=CARTESIAN_POINT('',(-0.195,-0.6,-2.38806125833734E-17)) ;
#24303=CARTESIAN_POINT('Origin',(0.,0.,0.)) ;
#24304=CARTESIAN_POINT('Origin',(0.,-1.2,0.)) ;
#24305=CARTESIAN_POINT('Origin',(0.,0.125,0.)) ;
#24306=CARTESIAN_POINT('',(-0.35,0.,-4.28626379701574E-17)) ;
#24307=CARTESIAN_POINT('Origin',(0.,0.,0.)) ;
#24308=CARTESIAN_POINT('',(-0.35,0.25,-4.28626379701574E-17)) ;
#24309=CARTESIAN_POINT('',(-0.35,0.125,-4.28626379701574E-17)) ;
#24310=CARTESIAN_POINT('Origin',(0.,0.25,0.)) ;
#24311=CARTESIAN_POINT('Origin',(0.,0.25,0.)) ;
#24312=CARTESIAN_POINT('Origin',(0.,0.,0.)) ;
#24574=UNCERTAINTY_MEASURE_WITH_UNIT(LENGTH_MEASURE(0.001),#24629,
'DISTANCE_ACCURACY_VALUE',
'Maximum model space distance between geometric entities at asserted c
onnectivities') ;
#24580=UNCERTAINTY_MEASURE_WITH_UNIT(LENGTH_MEASURE(0.001),#24629,
'DISTANCE_ACCURACY_VALUE',
'Maximum model space distance between geometric entities at asserted c
onnectivities') ;
#24622=(
GEOMETRIC_REPRESENTATION_CONTEXT(3)
GLOBAL_UNCERTAINTY_ASSIGNED_CONTEXT((#24574))
GLOBAL_UNIT_ASSIGNED_CONTEXT((#24629,#24631,#24632))
REPRESENTATION_CONTEXT('','3D')
) ;
#24628=(
GEOMETRIC_REPRESENTATION_CONTEXT(3)
GLOBAL_UNCERTAINTY_ASSIGNED_CONTEXT((#24580))
GLOBAL_UNIT_ASSIGNED_CONTEXT((#24629,#24631,#24632))
REPRESENTATION_CONTEXT('','3D')
) ;
#24629=(
LENGTH_UNIT()
NAMED_UNIT(*)
SI_UNIT(.CENTI.,.METRE.)
) ;
#24631=(
NAMED_UNIT(*)
PLANE_ANGLE_UNIT()
SI_UNIT($,.RADIAN.)
) ;
#24632=(
NAMED_UNIT(*)
SI_UNIT($,.STERADIAN.)
SOLID_ANGLE_UNIT()
) ;
#24674=SHAPE_DEFINITION_REPRESENTATION(#24762,#24832) ;
#24762=PRODUCT_DEFINITION_SHAPE('',$,#24880) ;
#24832=SHAPE_REPRESENTATION('',(#15298),#24622) ;
#24838=PRODUCT_DEFINITION_CONTEXT('part definition',#24981,'design') ;
#24880=PRODUCT_DEFINITION('HUB_SCREW_M4','HUB_SCREW_M4',#24927,
#24838) ;
#24927=PRODUCT_DEFINITION_FORMATION('',$,#25024) ;
#24981=APPLICATION_CONTEXT(
'Core Data for Automotive Mechanical Design Process') ;
#24982=PRODUCT_CONTEXT('part definition',#24981,'mechanical') ;
#25024=PRODUCT('HUB_SCREW_M4','HUB_SCREW_M4',$,(#24982)) ;
#25030=PRESENTATION_STYLE_ASSIGNMENT((#25040)) ;
#25040=SURFACE_STYLE_USAGE(.BOTH.,#25050) ;
#25050=SURFACE_SIDE_STYLE('',(#25060)) ;
#25060=SURFACE_STYLE_FILL_AREA(#25070) ;
#25070=FILL_AREA_STYLE('Steel - Satin',(#25080)) ;
#25080=FILL_AREA_STYLE_COLOUR('Steel - Satin',#25090) ;
#25090=COLOUR_RGB('Steel - Satin', 0.66274510, 0.83137255, 0.94901961) ;
ENDSEC;
END-ISO-10303-21;
